ISO-10303-21;
HEADER;
FILE_DESCRIPTION((''),'2;1');
FILE_NAME('Shaft Thrust Washer D24.4.step','2026-10-06T07:01:46+05:00',(''),(''),'','','');
FILE_SCHEMA (('AUTOMOTIVE_DESIGN { 1 0 10303 214 3 1 1 }'));
ENDSEC;
DATA;
#10=MECHANICAL_DESIGN_GEOMETRIC_PRESENTATION_REPRESENTATION('',(#147),#11396);
#117=SHAPE_REPRESENTATION_RELATIONSHIP('SRR','None',#11464,#132) ;
#132=ADVANCED_BREP_SHAPE_REPRESENTATION('',(#162),#11390) ;
#147=STYLED_ITEM('',(#11548),#162) ;
#162=MANIFOLD_SOLID_BREP('Shaft Thrust Washer D24.4',#5578) ;
#368=FACE_BOUND('',#1174,.T.) ;
#369=FACE_BOUND('',#1177,.T.) ;
#488=PLANE('',#6315) ;
#489=PLANE('',#6319) ;
#805=FACE_OUTER_BOUND('',#1172,.T.) ;
#806=FACE_OUTER_BOUND('',#1173,.T.) ;
#807=FACE_OUTER_BOUND('',#1175,.T.) ;
#808=FACE_OUTER_BOUND('',#1176,.T.) ;
#1172=EDGE_LOOP('',(#4930,#4931,#4932,#4933)) ;
#1173=EDGE_LOOP('',(#4934)) ;
#1174=EDGE_LOOP('',(#4935)) ;
#1175=EDGE_LOOP('',(#4936,#4937,#4938,#4939)) ;
#1176=EDGE_LOOP('',(#4940)) ;
#1177=EDGE_LOOP('',(#4941)) ;
#1561=LINE('',#11167,#1944) ;
#1562=LINE('',#11175,#1945) ;
#1944=VECTOR('',#7883,3.985) ;
#1945=VECTOR('',#7894,6.105) ;
#2231=CIRCLE('',#6313,3.985) ;
#2232=CIRCLE('',#6314,3.985) ;
#2233=CIRCLE('',#6316,6.105) ;
#2234=CIRCLE('',#6318,6.105) ;
#2692=VERTEX_POINT('',#11164) ;
#2693=VERTEX_POINT('',#11166) ;
#2694=VERTEX_POINT('',#11170) ;
#2695=VERTEX_POINT('',#11173) ;
#3447=EDGE_CURVE('',#2692,#2692,#2231,.T.) ;
#3448=EDGE_CURVE('',#2692,#2693,#1561,.T.) ;
#3449=EDGE_CURVE('',#2693,#2693,#2232,.T.) ;
#3450=EDGE_CURVE('',#2694,#2694,#2233,.T.) ;
#3451=EDGE_CURVE('',#2695,#2695,#2234,.T.) ;
#3452=EDGE_CURVE('',#2695,#2694,#1562,.T.) ;
#4930=ORIENTED_EDGE('',*,*,#3447,.T.) ;
#4931=ORIENTED_EDGE('',*,*,#3448,.T.) ;
#4932=ORIENTED_EDGE('',*,*,#3449,.F.) ;
#4933=ORIENTED_EDGE('',*,*,#3448,.F.) ;
#4934=ORIENTED_EDGE('',*,*,#3450,.F.) ;
#4935=ORIENTED_EDGE('',*,*,#3449,.T.) ;
#4936=ORIENTED_EDGE('',*,*,#3451,.F.) ;
#4937=ORIENTED_EDGE('',*,*,#3452,.T.) ;
#4938=ORIENTED_EDGE('',*,*,#3450,.T.) ;
#4939=ORIENTED_EDGE('',*,*,#3452,.F.) ;
#4940=ORIENTED_EDGE('',*,*,#3451,.T.) ;
#4941=ORIENTED_EDGE('',*,*,#3447,.F.) ;
#5214=CYLINDRICAL_SURFACE('',#6312,3.985) ;
#5215=CYLINDRICAL_SURFACE('',#6317,6.105) ;
#5530=ADVANCED_FACE('',(#805),#5214,.F.) ;
#5531=ADVANCED_FACE('',(#806,#368),#488,.T.) ;
#5532=ADVANCED_FACE('',(#807),#5215,.T.) ;
#5533=ADVANCED_FACE('',(#808,#369),#489,.T.) ;
#5578=CLOSED_SHELL('',(#5530,#5531,#5532,#5533)) ;
#6311=AXIS2_PLACEMENT_3D('',#11162,#7877,#7878) ;
#6312=AXIS2_PLACEMENT_3D('',#11163,#7879,#7880) ;
#6313=AXIS2_PLACEMENT_3D('',#11165,#7881,#7882) ;
#6314=AXIS2_PLACEMENT_3D('',#11168,#7884,#7885) ;
#6315=AXIS2_PLACEMENT_3D('',#11169,#7886,#7887) ;
#6316=AXIS2_PLACEMENT_3D('',#11171,#7888,#7889) ;
#6317=AXIS2_PLACEMENT_3D('',#11172,#7890,#7891) ;
#6318=AXIS2_PLACEMENT_3D('',#11174,#7892,#7893) ;
#6319=AXIS2_PLACEMENT_3D('',#11176,#7895,#7896) ;
#7877=DIRECTION('axis',(0.,0.,1.)) ;
#7878=DIRECTION('refdir',(1.,0.,0.)) ;
#7879=DIRECTION('center_axis',(1.,0.,0.)) ;
#7880=DIRECTION('ref_axis',(0.,1.,0.)) ;
#7881=DIRECTION('center_axis',(1.,0.,0.)) ;
#7882=DIRECTION('ref_axis',(0.,0.,-1.)) ;
#7883=DIRECTION('',(-1.,0.,0.)) ;
#7884=DIRECTION('center_axis',(1.,0.,0.)) ;
#7885=DIRECTION('ref_axis',(0.,0.,-1.)) ;
#7886=DIRECTION('center_axis',(-1.,0.,0.)) ;
#7887=DIRECTION('ref_axis',(0.,0.,1.)) ;
#7888=DIRECTION('center_axis',(1.,0.,0.)) ;
#7889=DIRECTION('ref_axis',(0.,0.,-1.)) ;
#7890=DIRECTION('center_axis',(1.,0.,0.)) ;
#7891=DIRECTION('ref_axis',(0.,1.,0.)) ;
#7892=DIRECTION('center_axis',(1.,0.,0.)) ;
#7893=DIRECTION('ref_axis',(0.,0.,-1.)) ;
#7894=DIRECTION('',(-1.,0.,0.)) ;
#7895=DIRECTION('center_axis',(1.,0.,0.)) ;
#7896=DIRECTION('ref_axis',(0.,0.,-1.)) ;
#11162=CARTESIAN_POINT('',(0.,0.,0.)) ;
#11163=CARTESIAN_POINT('Origin',(-25.0225,17.565,27.14)) ;
#11164=CARTESIAN_POINT('',(-24.705,13.58,27.14)) ;
#11165=CARTESIAN_POINT('Origin',(-24.705,17.565,27.14)) ;
#11166=CARTESIAN_POINT('',(-25.34,13.58,27.14)) ;
#11167=CARTESIAN_POINT('',(-25.0225,13.58,27.14)) ;
#11168=CARTESIAN_POINT('Origin',(-25.34,17.565,27.14)) ;
#11169=CARTESIAN_POINT('Origin',(-25.34,23.67,27.14)) ;
#11170=CARTESIAN_POINT('',(-25.34,11.46,27.14)) ;
#11171=CARTESIAN_POINT('Origin',(-25.34,17.565,27.14)) ;
#11172=CARTESIAN_POINT('Origin',(-25.0225,17.565,27.14)) ;
#11173=CARTESIAN_POINT('',(-24.705,11.46,27.14)) ;
#11174=CARTESIAN_POINT('Origin',(-24.705,17.565,27.14)) ;
#11175=CARTESIAN_POINT('',(-25.0225,11.46,27.14)) ;
#11176=CARTESIAN_POINT('Origin',(-24.705,21.55,27.14)) ;
#11373=UNCERTAINTY_MEASURE_WITH_UNIT(LENGTH_MEASURE(0.01),#11397,
'DISTANCE_ACCURACY_VALUE',
'Maximum model space distance between geometric entities at asserted c
onnectivities') ;
#11379=UNCERTAINTY_MEASURE_WITH_UNIT(LENGTH_MEASURE(0.01),#11397,
'DISTANCE_ACCURACY_VALUE',
'Maximum model space distance between geometric entities at asserted c
onnectivities') ;
#11390=(
GEOMETRIC_REPRESENTATION_CONTEXT(3)
GLOBAL_UNCERTAINTY_ASSIGNED_CONTEXT((#11373))
GLOBAL_UNIT_ASSIGNED_CONTEXT((#11397,#11399,#11400))
REPRESENTATION_CONTEXT('','3D')
) ;
#11396=(
GEOMETRIC_REPRESENTATION_CONTEXT(3)
GLOBAL_UNCERTAINTY_ASSIGNED_CONTEXT((#11379))
GLOBAL_UNIT_ASSIGNED_CONTEXT((#11397,#11399,#11400))
REPRESENTATION_CONTEXT('','3D')
) ;
#11397=(
LENGTH_UNIT()
NAMED_UNIT(*)
SI_UNIT(.MILLI.,.METRE.)
) ;
#11399=(
NAMED_UNIT(*)
PLANE_ANGLE_UNIT()
SI_UNIT($,.RADIAN.)
) ;
#11400=(
NAMED_UNIT(*)
SI_UNIT($,.STERADIAN.)
SOLID_ANGLE_UNIT()
) ;
#11411=SHAPE_DEFINITION_REPRESENTATION(#11427,#11464) ;
#11427=PRODUCT_DEFINITION_SHAPE('',$,#11481) ;
#11464=SHAPE_REPRESENTATION('',(#6311),#11390) ;
#11470=PRODUCT_DEFINITION_CONTEXT('part definition',#11520,'design') ;
#11481=PRODUCT_DEFINITION('Shaft Thrust Washer D24.4',
'Shaft Thrust Washer D24.4',#11497,#11470) ;
#11497=PRODUCT_DEFINITION_FORMATION('',$,#11532) ;
#11520=APPLICATION_CONTEXT(
'Core Data for Automotive Mechanical Design Process') ;
#11521=PRODUCT_CONTEXT('part definition',#11520,'mechanical') ;
#11532=PRODUCT('Shaft Thrust Washer D24.4','Shaft Thrust Washer D24.4',$,
(#11521)) ;
#11548=PRESENTATION_STYLE_ASSIGNMENT((#11564)) ;
#11564=SURFACE_STYLE_USAGE(.BOTH.,#11580) ;
#11580=SURFACE_SIDE_STYLE('',(#11596)) ;
#11596=SURFACE_STYLE_FILL_AREA(#11612) ;
#11612=FILL_AREA_STYLE('MAS-252 Metallic - Shaft Thrust Washer D24.4',(#11628)) ;
#11628=FILL_AREA_STYLE_COLOUR(
'MAS-252 Metallic - Shaft Thrust Washer D24.4',#11644) ;
#11644=COLOUR_RGB('MAS-252 Metallic - Shaft Thrust Washer D24.4', 0.40784314, 0.44705882, 0.49803922) ;
ENDSEC;
END-ISO-10303-21;
